ISO-10303-21;
HEADER;
/* Generated by software containing ST-Developer
 * from STEP Tools, Inc. (www.steptools.com) 
 */

FILE_DESCRIPTION(
/* description */ ('Belt conveyor head drive unit'),
/* implementation_level */ '2;1');

FILE_NAME(
/* name */ 'M4 clamp nut (1).step',
/* time_stamp */ '2026-10-28T03:26:19-07:00',
/* author */ (''),
/* organization */ (''),
/* preprocessor_version */ 'ST-DEVELOPER v20.2',
/* originating_system */ 'Autodesk Translation Framework v15.17.0.0',
/* authorisation */ '');

FILE_SCHEMA (('AUTOMOTIVE_DESIGN { 1 0 10303 214 3 1 1 }'));
ENDSEC;

DATA;
#10=MECHANICAL_DESIGN_GEOMETRIC_PRESENTATION_REPRESENTATION('',(#856),#27069);
#718=SHAPE_REPRESENTATION_RELATIONSHIP('SRR','None',#27362,#787);
#787=ADVANCED_BREP_SHAPE_REPRESENTATION('',(#941),#27004);
#856=STYLED_ITEM('',(#27804),#941);
#941=MANIFOLD_SOLID_BREP('Body1',#13721);
#1078=FACE_BOUND('',#2642,.T.);
#1079=FACE_BOUND('',#2644,.T.);
#1350=PLANE('',#14858);
#1351=PLANE('',#14859);
#1773=FACE_OUTER_BOUND('',#2639,.T.);
#1774=FACE_OUTER_BOUND('',#2640,.T.);
#1775=FACE_OUTER_BOUND('',#2641,.T.);
#1776=FACE_OUTER_BOUND('',#2643,.T.);
#2639=EDGE_LOOP('',(#9606,#9607,#9608,#9609));
#2640=EDGE_LOOP('',(#9610,#9611,#9612,#9613));
#2641=EDGE_LOOP('',(#9614));
#2642=EDGE_LOOP('',(#9615));
#2643=EDGE_LOOP('',(#9616));
#2644=EDGE_LOOP('',(#9617));
#3684=LINE('',#21666,#4476);
#3685=LINE('',#21672,#4477);
#4476=VECTOR('',#17204,0.165);
#4477=VECTOR('',#17211,0.4);
#5220=CIRCLE('',#14853,0.165);
#5221=CIRCLE('',#14854,0.165);
#5222=CIRCLE('',#14856,0.4);
#5223=CIRCLE('',#14857,0.4);
#6169=VERTEX_POINT('',#21663);
#6170=VERTEX_POINT('',#21665);
#6171=VERTEX_POINT('',#21669);
#6172=VERTEX_POINT('',#21671);
#7495=EDGE_CURVE('',#6169,#6169,#5220,.T.);
#7496=EDGE_CURVE('',#6169,#6170,#3684,.T.);
#7497=EDGE_CURVE('',#6170,#6170,#5221,.T.);
#7498=EDGE_CURVE('',#6171,#6171,#5222,.T.);
#7499=EDGE_CURVE('',#6171,#6172,#3685,.T.);
#7500=EDGE_CURVE('',#6172,#6172,#5223,.T.);
#9606=ORIENTED_EDGE('',*,*,#7495,.F.);
#9607=ORIENTED_EDGE('',*,*,#7496,.T.);
#9608=ORIENTED_EDGE('',*,*,#7497,.T.);
#9609=ORIENTED_EDGE('',*,*,#7496,.F.);
#9610=ORIENTED_EDGE('',*,*,#7498,.F.);
#9611=ORIENTED_EDGE('',*,*,#7499,.T.);
#9612=ORIENTED_EDGE('',*,*,#7500,.T.);
#9613=ORIENTED_EDGE('',*,*,#7499,.F.);
#9614=ORIENTED_EDGE('',*,*,#7498,.T.);
#9615=ORIENTED_EDGE('',*,*,#7495,.T.);
#9616=ORIENTED_EDGE('',*,*,#7500,.F.);
#9617=ORIENTED_EDGE('',*,*,#7497,.F.);
#12599=CYLINDRICAL_SURFACE('',#14852,0.165);
#12600=CYLINDRICAL_SURFACE('',#14855,0.4);
#13052=ADVANCED_FACE('',(#1773),#12599,.F.);
#13053=ADVANCED_FACE('',(#1774),#12600,.T.);
#13054=ADVANCED_FACE('',(#1775,#1078),#1350,.T.);
#13055=ADVANCED_FACE('',(#1776,#1079),#1351,.F.);
#13721=CLOSED_SHELL('',(#13052,#13053,#13054,#13055));
#14851=AXIS2_PLACEMENT_3D('',#21661,#17198,#17199);
#14852=AXIS2_PLACEMENT_3D('',#21662,#17200,#17201);
#14853=AXIS2_PLACEMENT_3D('',#21664,#17202,#17203);
#14854=AXIS2_PLACEMENT_3D('',#21667,#17205,#17206);
#14855=AXIS2_PLACEMENT_3D('',#21668,#17207,#17208);
#14856=AXIS2_PLACEMENT_3D('',#21670,#17209,#17210);
#14857=AXIS2_PLACEMENT_3D('',#21673,#17212,#17213);
#14858=AXIS2_PLACEMENT_3D('',#21674,#17214,#17215);
#14859=AXIS2_PLACEMENT_3D('',#21675,#17216,#17217);
#17198=DIRECTION('axis',(0.,0.,1.));
#17199=DIRECTION('refdir',(1.,0.,0.));
#17200=DIRECTION('center_axis',(0.,0.,1.));
#17201=DIRECTION('ref_axis',(1.,0.,0.));
#17202=DIRECTION('center_axis',(0.,0.,-1.));
#17203=DIRECTION('ref_axis',(1.,0.,0.));
#17204=DIRECTION('',(0.,0.,-1.));
#17205=DIRECTION('center_axis',(0.,0.,-1.));
#17206=DIRECTION('ref_axis',(1.,0.,0.));
#17207=DIRECTION('center_axis',(0.,0.,1.));
#17208=DIRECTION('ref_axis',(1.,0.,0.));
#17209=DIRECTION('center_axis',(0.,0.,1.));
#17210=DIRECTION('ref_axis',(1.,0.,0.));
#17211=DIRECTION('',(0.,0.,-1.));
#17212=DIRECTION('center_axis',(0.,0.,1.));
#17213=DIRECTION('ref_axis',(1.,0.,0.));
#17214=DIRECTION('center_axis',(0.,0.,1.));
#17215=DIRECTION('ref_axis',(1.,0.,0.));
#17216=DIRECTION('center_axis',(0.,0.,1.));
#17217=DIRECTION('ref_axis',(1.,0.,0.));
#21661=CARTESIAN_POINT('',(0.,0.,0.));
#21662=CARTESIAN_POINT('Origin',(4.17091003018116,1.,-1.6));
#21663=CARTESIAN_POINT('',(4.00591003018116,1.,-1.2));
#21664=CARTESIAN_POINT('Origin',(4.17091003018116,1.,-1.2));
#21665=CARTESIAN_POINT('',(4.00591003018116,1.,-1.6));
#21666=CARTESIAN_POINT('',(4.00591003018116,1.,-1.6));
#21667=CARTESIAN_POINT('Origin',(4.17091003018116,1.,-1.6));
#21668=CARTESIAN_POINT('Origin',(4.17091003018116,1.,-1.6));
#21669=CARTESIAN_POINT('',(3.77091003018116,1.,-1.2));
#21670=CARTESIAN_POINT('Origin',(4.17091003018116,1.,-1.2));
#21671=CARTESIAN_POINT('',(3.77091003018116,1.,-1.6));
#21672=CARTESIAN_POINT('',(3.77091003018116,1.,-1.6));
#21673=CARTESIAN_POINT('Origin',(4.17091003018116,1.,-1.6));
#21674=CARTESIAN_POINT('Origin',(4.17091003018116,1.,-1.2));
#21675=CARTESIAN_POINT('Origin',(4.17091003018116,1.,-1.6));
#26927=UNCERTAINTY_MEASURE_WITH_UNIT(LENGTH_MEASURE(0.001),#27070,
'DISTANCE_ACCURACY_VALUE',
'Maximum model space distance between geometric entities at asserted c
onnectivities');
#26992=UNCERTAINTY_MEASURE_WITH_UNIT(LENGTH_MEASURE(0.001),#27070,
'DISTANCE_ACCURACY_VALUE',
'Maximum model space distance between geometric entities at asserted c
onnectivities');
#27004=(
GEOMETRIC_REPRESENTATION_CONTEXT(3)
GLOBAL_UNCERTAINTY_ASSIGNED_CONTEXT((#26927))
GLOBAL_UNIT_ASSIGNED_CONTEXT((#27070,#27072,#27073))
REPRESENTATION_CONTEXT('','3D')
);
#27069=(
GEOMETRIC_REPRESENTATION_CONTEXT(3)
GLOBAL_UNCERTAINTY_ASSIGNED_CONTEXT((#26992))
GLOBAL_UNIT_ASSIGNED_CONTEXT((#27070,#27072,#27073))
REPRESENTATION_CONTEXT('','3D')
);
#27070=(
LENGTH_UNIT()
NAMED_UNIT(*)
SI_UNIT(.CENTI.,.METRE.)
);
#27072=(
NAMED_UNIT(*)
PLANE_ANGLE_UNIT()
SI_UNIT($,.RADIAN.)
);
#27073=(
NAMED_UNIT(*)
SI_UNIT($,.STERADIAN.)
SOLID_ANGLE_UNIT()
);
#27085=SHAPE_DEFINITION_REPRESENTATION(#27161,#27362);
#27161=PRODUCT_DEFINITION_SHAPE('',$,#27439);
#27362=SHAPE_REPRESENTATION('',(#14851),#27004);
#27427=PRODUCT_DEFINITION_CONTEXT('part definition',#27657,'design');
#27439=PRODUCT_DEFINITION('M4 clamp nut (1)','M4 clamp nut (1)',#27515,#27427);
#27515=PRODUCT_DEFINITION_FORMATION('',$,#27670);
#27657=APPLICATION_CONTEXT(
'Core Data for Automotive Mechanical Design Process');
#27658=PRODUCT_CONTEXT('part definition',#27657,'mechanical');
#27670=PRODUCT('M4 clamp nut (1)','M4 clamp nut (1)','M4 clamp nut (1)',(#27658));
#27798=COLOUR_RGB('Black',0.12,0.14,0.17);
#27799=FILL_AREA_STYLE_COLOUR('',#27798);
#27800=FILL_AREA_STYLE('',(#27799));
#27801=SURFACE_STYLE_FILL_AREA(#27800);
#27802=SURFACE_SIDE_STYLE('',(#27801));
#27803=SURFACE_STYLE_USAGE(.BOTH.,#27802);
#27804=PRESENTATION_STYLE_ASSIGNMENT((#27803));
ENDSEC;
END-ISO-10303-21;
